ISO-10303-21;
HEADER;
/* Generated by software containing ST-Developer
 * from STEP Tools, Inc. (www.steptools.com) 
 */

FILE_DESCRIPTION(
/* description */ ('Wall-mounted air drop station'),
/* implementation_level */ '2;1');

FILE_NAME(
/* name */ 'Cap Screw - M4x16.step',
/* time_stamp */ '2026-10-28T22:16:19-07:00',
/* author */ (''),
/* organization */ (''),
/* preprocessor_version */ 'ST-DEVELOPER v20.2',
/* originating_system */ 'Autodesk Translation Framework v15.17.0.0',
/* authorisation */ '');

FILE_SCHEMA (('AUTOMOTIVE_DESIGN { 1 0 10303 214 3 1 1 }'));
ENDSEC;

DATA;
#10=MECHANICAL_DESIGN_GEOMETRIC_PRESENTATION_REPRESENTATION('',(#362),#10517);
#252=ORIENTED_CLOSED_SHELL('',*,#5903,.F.);
#255=BREP_WITH_VOIDS('Body1',#5902,(#252));
#275=CONICAL_SURFACE('',#6656,0.325,0.785398163397448);
#276=CONICAL_SURFACE('',#6660,0.335,0.785398163397448);
#277=CONICAL_SURFACE('',#6664,0.21,0.463647609000806);
#278=CONICAL_SURFACE('',#6668,0.18,0.785398163397448);
#304=SHAPE_REPRESENTATION_RELATIONSHIP('SRR','None',#10661,#333);
#333=ADVANCED_BREP_SHAPE_REPRESENTATION('',(#255),#10505);
#362=STYLED_ITEM('',(#10881),#255);
#504=FACE_BOUND('',#1447,.T.);
#663=PLANE('',#6654);
#664=PLANE('',#6662);
#665=PLANE('',#6670);
#666=PLANE('',#6671);
#667=PLANE('',#6672);
#668=PLANE('',#6673);
#669=PLANE('',#6674);
#670=PLANE('',#6675);
#671=PLANE('',#6676);
#672=PLANE('',#6677);
#673=PLANE('',#6678);
#982=FACE_OUTER_BOUND('',#1442,.T.);
#983=FACE_OUTER_BOUND('',#1443,.T.);
#984=FACE_OUTER_BOUND('',#1444,.T.);
#985=FACE_OUTER_BOUND('',#1445,.T.);
#986=FACE_OUTER_BOUND('',#1446,.T.);
#987=FACE_OUTER_BOUND('',#1448,.T.);
#988=FACE_OUTER_BOUND('',#1449,.T.);
#989=FACE_OUTER_BOUND('',#1450,.T.);
#990=FACE_OUTER_BOUND('',#1451,.T.);
#991=FACE_OUTER_BOUND('',#1452,.T.);
#992=FACE_OUTER_BOUND('',#1453,.T.);
#993=FACE_OUTER_BOUND('',#1454,.T.);
#994=FACE_OUTER_BOUND('',#1455,.T.);
#995=FACE_OUTER_BOUND('',#1456,.T.);
#996=FACE_OUTER_BOUND('',#1457,.T.);
#997=FACE_OUTER_BOUND('',#1458,.T.);
#998=FACE_OUTER_BOUND('',#1459,.T.);
#1442=EDGE_LOOP('',(#4917));
#1443=EDGE_LOOP('',(#4918,#4919,#4920,#4921));
#1444=EDGE_LOOP('',(#4922,#4923,#4924,#4925));
#1445=EDGE_LOOP('',(#4926,#4927,#4928,#4929));
#1446=EDGE_LOOP('',(#4930));
#1447=EDGE_LOOP('',(#4931));
#1448=EDGE_LOOP('',(#4932,#4933,#4934,#4935));
#1449=EDGE_LOOP('',(#4936,#4937,#4938,#4939));
#1450=EDGE_LOOP('',(#4940,#4941,#4942,#4943));
#1451=EDGE_LOOP('',(#4944));
#1452=EDGE_LOOP('',(#4945,#4946,#4947,#4948));
#1453=EDGE_LOOP('',(#4949,#4950,#4951,#4952));
#1454=EDGE_LOOP('',(#4953,#4954,#4955,#4956));
#1455=EDGE_LOOP('',(#4957,#4958,#4959,#4960));
#1456=EDGE_LOOP('',(#4961,#4962,#4963,#4964));
#1457=EDGE_LOOP('',(#4965,#4966,#4967,#4968));
#1458=EDGE_LOOP('',(#4969,#4970,#4971,#4972,#4973,#4974));
#1459=EDGE_LOOP('',(#4975,#4976,#4977,#4978,#4979,#4980));
#1881=LINE('',#9828,#2345);
#1882=LINE('',#9832,#2346);
#1883=LINE('',#9836,#2347);
#1884=LINE('',#9843,#2348);
#1885=LINE('',#9847,#2349);
#1886=LINE('',#9851,#2350);
#1887=LINE('',#9856,#2351);
#1888=LINE('',#9858,#2352);
#1889=LINE('',#9860,#2353);
#1890=LINE('',#9861,#2354);
#1891=LINE('',#9864,#2355);
#1892=LINE('',#9866,#2356);
#1893=LINE('',#9867,#2357);
#1894=LINE('',#9870,#2358);
#1895=LINE('',#9872,#2359);
#1896=LINE('',#9873,#2360);
#1897=LINE('',#9876,#2361);
#1898=LINE('',#9878,#2362);
#1899=LINE('',#9879,#2363);
#1900=LINE('',#9882,#2364);
#1901=LINE('',#9884,#2365);
#1902=LINE('',#9885,#2366);
#1903=LINE('',#9887,#2367);
#1904=LINE('',#9888,#2368);
#2345=VECTOR('',#8059,0.325);
#2346=VECTOR('',#8064,0.35);
#2347=VECTOR('',#8069,0.335);
#2348=VECTOR('',#8078,0.21);
#2349=VECTOR('',#8083,0.2);
#2350=VECTOR('',#8088,0.18);
#2351=VECTOR('',#8093,1.);
#2352=VECTOR('',#8094,1.);
#2353=VECTOR('',#8095,1.);
#2354=VECTOR('',#8096,1.);
#2355=VECTOR('',#8099,1.);
#2356=VECTOR('',#8100,1.);
#2357=VECTOR('',#8101,1.);
#2358=VECTOR('',#8104,1.);
#2359=VECTOR('',#8105,1.);
#2360=VECTOR('',#8106,1.);
#2361=VECTOR('',#8109,1.);
#2362=VECTOR('',#8110,1.);
#2363=VECTOR('',#8111,1.);
#2364=VECTOR('',#8114,1.);
#2365=VECTOR('',#8115,1.);
#2366=VECTOR('',#8116,1.);
#2367=VECTOR('',#8119,1.);
#2368=VECTOR('',#8120,1.);
#2691=CIRCLE('',#6655,0.3);
#2692=CIRCLE('',#6657,0.35);
#2693=CIRCLE('',#6659,0.35);
#2694=CIRCLE('',#6661,0.32);
#2695=CIRCLE('',#6663,0.22);
#2696=CIRCLE('',#6665,0.1954);
#2697=CIRCLE('',#6667,0.1954);
#2698=CIRCLE('',#6669,0.16);
#3077=VERTEX_POINT('',#9823);
#3078=VERTEX_POINT('',#9826);
#3079=VERTEX_POINT('',#9830);
#3080=VERTEX_POINT('',#9834);
#3081=VERTEX_POINT('',#9838);
#3082=VERTEX_POINT('',#9841);
#3083=VERTEX_POINT('',#9845);
#3084=VERTEX_POINT('',#9849);
#3085=VERTEX_POINT('',#9854);
#3086=VERTEX_POINT('',#9855);
#3087=VERTEX_POINT('',#9857);
#3088=VERTEX_POINT('',#9859);
#3089=VERTEX_POINT('',#9863);
#3090=VERTEX_POINT('',#9865);
#3091=VERTEX_POINT('',#9869);
#3092=VERTEX_POINT('',#9871);
#3093=VERTEX_POINT('',#9875);
#3094=VERTEX_POINT('',#9877);
#3095=VERTEX_POINT('',#9881);
#3096=VERTEX_POINT('',#9883);
#3716=EDGE_CURVE('',#3077,#3077,#2691,.T.);
#3717=EDGE_CURVE('',#3078,#3078,#2692,.T.);
#3718=EDGE_CURVE('',#3078,#3077,#1881,.T.);
#3719=EDGE_CURVE('',#3079,#3079,#2693,.T.);
#3720=EDGE_CURVE('',#3079,#3078,#1882,.T.);
#3721=EDGE_CURVE('',#3080,#3080,#2694,.T.);
#3722=EDGE_CURVE('',#3080,#3079,#1883,.T.);
#3723=EDGE_CURVE('',#3081,#3081,#2695,.T.);
#3724=EDGE_CURVE('',#3082,#3082,#2696,.F.);
#3725=EDGE_CURVE('',#3082,#3081,#1884,.T.);
#3726=EDGE_CURVE('',#3083,#3083,#2697,.F.);
#3727=EDGE_CURVE('',#3083,#3082,#1885,.T.);
#3728=EDGE_CURVE('',#3084,#3084,#2698,.T.);
#3729=EDGE_CURVE('',#3084,#3083,#1886,.T.);
#3730=EDGE_CURVE('',#3085,#3086,#1887,.T.);
#3731=EDGE_CURVE('',#3086,#3087,#1888,.T.);
#3732=EDGE_CURVE('',#3087,#3088,#1889,.T.);
#3733=EDGE_CURVE('',#3085,#3088,#1890,.T.);
#3734=EDGE_CURVE('',#3086,#3089,#1891,.T.);
#3735=EDGE_CURVE('',#3089,#3090,#1892,.T.);
#3736=EDGE_CURVE('',#3090,#3087,#1893,.T.);
#3737=EDGE_CURVE('',#3089,#3091,#1894,.T.);
#3738=EDGE_CURVE('',#3091,#3092,#1895,.T.);
#3739=EDGE_CURVE('',#3092,#3090,#1896,.T.);
#3740=EDGE_CURVE('',#3091,#3093,#1897,.T.);
#3741=EDGE_CURVE('',#3093,#3094,#1898,.T.);
#3742=EDGE_CURVE('',#3094,#3092,#1899,.T.);
#3743=EDGE_CURVE('',#3093,#3095,#1900,.T.);
#3744=EDGE_CURVE('',#3095,#3096,#1901,.T.);
#3745=EDGE_CURVE('',#3096,#3094,#1902,.T.);
#3746=EDGE_CURVE('',#3095,#3085,#1903,.T.);
#3747=EDGE_CURVE('',#3088,#3096,#1904,.T.);
#4917=ORIENTED_EDGE('',*,*,#3716,.F.);
#4918=ORIENTED_EDGE('',*,*,#3717,.F.);
#4919=ORIENTED_EDGE('',*,*,#3718,.T.);
#4920=ORIENTED_EDGE('',*,*,#3716,.T.);
#4921=ORIENTED_EDGE('',*,*,#3718,.F.);
#4922=ORIENTED_EDGE('',*,*,#3719,.F.);
#4923=ORIENTED_EDGE('',*,*,#3720,.T.);
#4924=ORIENTED_EDGE('',*,*,#3717,.T.);
#4925=ORIENTED_EDGE('',*,*,#3720,.F.);
#4926=ORIENTED_EDGE('',*,*,#3721,.F.);
#4927=ORIENTED_EDGE('',*,*,#3722,.T.);
#4928=ORIENTED_EDGE('',*,*,#3719,.T.);
#4929=ORIENTED_EDGE('',*,*,#3722,.F.);
#4930=ORIENTED_EDGE('',*,*,#3721,.T.);
#4931=ORIENTED_EDGE('',*,*,#3723,.F.);
#4932=ORIENTED_EDGE('',*,*,#3724,.F.);
#4933=ORIENTED_EDGE('',*,*,#3725,.T.);
#4934=ORIENTED_EDGE('',*,*,#3723,.T.);
#4935=ORIENTED_EDGE('',*,*,#3725,.F.);
#4936=ORIENTED_EDGE('',*,*,#3726,.F.);
#4937=ORIENTED_EDGE('',*,*,#3727,.T.);
#4938=ORIENTED_EDGE('',*,*,#3724,.T.);
#4939=ORIENTED_EDGE('',*,*,#3727,.F.);
#4940=ORIENTED_EDGE('',*,*,#3728,.F.);
#4941=ORIENTED_EDGE('',*,*,#3729,.T.);
#4942=ORIENTED_EDGE('',*,*,#3726,.T.);
#4943=ORIENTED_EDGE('',*,*,#3729,.F.);
#4944=ORIENTED_EDGE('',*,*,#3728,.T.);
#4945=ORIENTED_EDGE('',*,*,#3730,.T.);
#4946=ORIENTED_EDGE('',*,*,#3731,.T.);
#4947=ORIENTED_EDGE('',*,*,#3732,.T.);
#4948=ORIENTED_EDGE('',*,*,#3733,.F.);
#4949=ORIENTED_EDGE('',*,*,#3734,.T.);
#4950=ORIENTED_EDGE('',*,*,#3735,.T.);
#4951=ORIENTED_EDGE('',*,*,#3736,.T.);
#4952=ORIENTED_EDGE('',*,*,#3731,.F.);
#4953=ORIENTED_EDGE('',*,*,#3737,.T.);
#4954=ORIENTED_EDGE('',*,*,#3738,.T.);
#4955=ORIENTED_EDGE('',*,*,#3739,.T.);
#4956=ORIENTED_EDGE('',*,*,#3735,.F.);
#4957=ORIENTED_EDGE('',*,*,#3740,.T.);
#4958=ORIENTED_EDGE('',*,*,#3741,.T.);
#4959=ORIENTED_EDGE('',*,*,#3742,.T.);
#4960=ORIENTED_EDGE('',*,*,#3738,.F.);
#4961=ORIENTED_EDGE('',*,*,#3743,.T.);
#4962=ORIENTED_EDGE('',*,*,#3744,.T.);
#4963=ORIENTED_EDGE('',*,*,#3745,.T.);
#4964=ORIENTED_EDGE('',*,*,#3741,.F.);
#4965=ORIENTED_EDGE('',*,*,#3746,.T.);
#4966=ORIENTED_EDGE('',*,*,#3733,.T.);
#4967=ORIENTED_EDGE('',*,*,#3747,.T.);
#4968=ORIENTED_EDGE('',*,*,#3744,.F.);
#4969=ORIENTED_EDGE('',*,*,#3746,.F.);
#4970=ORIENTED_EDGE('',*,*,#3743,.F.);
#4971=ORIENTED_EDGE('',*,*,#3740,.F.);
#4972=ORIENTED_EDGE('',*,*,#3737,.F.);
#4973=ORIENTED_EDGE('',*,*,#3734,.F.);
#4974=ORIENTED_EDGE('',*,*,#3730,.F.);
#4975=ORIENTED_EDGE('',*,*,#3747,.F.);
#4976=ORIENTED_EDGE('',*,*,#3732,.F.);
#4977=ORIENTED_EDGE('',*,*,#3736,.F.);
#4978=ORIENTED_EDGE('',*,*,#3739,.F.);
#4979=ORIENTED_EDGE('',*,*,#3742,.F.);
#4980=ORIENTED_EDGE('',*,*,#3745,.F.);
#5506=CYLINDRICAL_SURFACE('',#6658,0.35);
#5507=CYLINDRICAL_SURFACE('',#6666,0.1954);
#5755=ADVANCED_FACE('',(#982),#663,.T.);
#5756=ADVANCED_FACE('',(#983),#275,.T.);
#5757=ADVANCED_FACE('',(#984),#5506,.T.);
#5758=ADVANCED_FACE('',(#985),#276,.T.);
#5759=ADVANCED_FACE('',(#986,#504),#664,.T.);
#5760=ADVANCED_FACE('',(#987),#277,.T.);
#5761=ADVANCED_FACE('',(#988),#5507,.T.);
#5762=ADVANCED_FACE('',(#989),#278,.T.);
#5763=ADVANCED_FACE('',(#990),#665,.T.);
#5764=ADVANCED_FACE('',(#991),#666,.F.);
#5765=ADVANCED_FACE('',(#992),#667,.F.);
#5766=ADVANCED_FACE('',(#993),#668,.F.);
#5767=ADVANCED_FACE('',(#994),#669,.F.);
#5768=ADVANCED_FACE('',(#995),#670,.F.);
#5769=ADVANCED_FACE('',(#996),#671,.F.);
#5770=ADVANCED_FACE('',(#997),#672,.F.);
#5771=ADVANCED_FACE('',(#998),#673,.F.);
#5902=CLOSED_SHELL('',(#5755,#5756,#5757,#5758,#5759,#5760,#5761,#5762,
#5763));
#5903=CLOSED_SHELL('',(#5764,#5765,#5766,#5767,#5768,#5769,#5770,#5771));
#6653=AXIS2_PLACEMENT_3D('',#9821,#8049,#8050);
#6654=AXIS2_PLACEMENT_3D('',#9822,#8051,#8052);
#6655=AXIS2_PLACEMENT_3D('',#9824,#8053,#8054);
#6656=AXIS2_PLACEMENT_3D('',#9825,#8055,#8056);
#6657=AXIS2_PLACEMENT_3D('',#9827,#8057,#8058);
#6658=AXIS2_PLACEMENT_3D('',#9829,#8060,#8061);
#6659=AXIS2_PLACEMENT_3D('',#9831,#8062,#8063);
#6660=AXIS2_PLACEMENT_3D('',#9833,#8065,#8066);
#6661=AXIS2_PLACEMENT_3D('',#9835,#8067,#8068);
#6662=AXIS2_PLACEMENT_3D('',#9837,#8070,#8071);
#6663=AXIS2_PLACEMENT_3D('',#9839,#8072,#8073);
#6664=AXIS2_PLACEMENT_3D('',#9840,#8074,#8075);
#6665=AXIS2_PLACEMENT_3D('',#9842,#8076,#8077);
#6666=AXIS2_PLACEMENT_3D('',#9844,#8079,#8080);
#6667=AXIS2_PLACEMENT_3D('',#9846,#8081,#8082);
#6668=AXIS2_PLACEMENT_3D('',#9848,#8084,#8085);
#6669=AXIS2_PLACEMENT_3D('',#9850,#8086,#8087);
#6670=AXIS2_PLACEMENT_3D('',#9852,#8089,#8090);
#6671=AXIS2_PLACEMENT_3D('',#9853,#8091,#8092);
#6672=AXIS2_PLACEMENT_3D('',#9862,#8097,#8098);
#6673=AXIS2_PLACEMENT_3D('',#9868,#8102,#8103);
#6674=AXIS2_PLACEMENT_3D('',#9874,#8107,#8108);
#6675=AXIS2_PLACEMENT_3D('',#9880,#8112,#8113);
#6676=AXIS2_PLACEMENT_3D('',#9886,#8117,#8118);
#6677=AXIS2_PLACEMENT_3D('',#9889,#8121,#8122);
#6678=AXIS2_PLACEMENT_3D('',#9890,#8123,#8124);
#8049=DIRECTION('axis',(0.,0.,1.));
#8050=DIRECTION('refdir',(1.,0.,0.));
#8051=DIRECTION('center_axis',(0.,1.,0.));
#8052=DIRECTION('ref_axis',(0.,0.,1.));
#8053=DIRECTION('center_axis',(0.,-1.,0.));
#8054=DIRECTION('ref_axis',(1.,0.,0.));
#8055=DIRECTION('center_axis',(0.,-1.,0.));
#8056=DIRECTION('ref_axis',(1.,0.,0.));
#8057=DIRECTION('center_axis',(0.,-1.,0.));
#8058=DIRECTION('ref_axis',(1.,0.,0.));
#8059=DIRECTION('',(0.707106781186547,0.707106781186548,8.65956056235493E-17));
#8060=DIRECTION('center_axis',(0.,-1.,0.));
#8061=DIRECTION('ref_axis',(1.,0.,0.));
#8062=DIRECTION('center_axis',(0.,-1.,0.));
#8063=DIRECTION('ref_axis',(1.,0.,0.));
#8064=DIRECTION('',(0.,1.,0.));
#8065=DIRECTION('center_axis',(0.,1.,0.));
#8066=DIRECTION('ref_axis',(1.,0.,0.));
#8067=DIRECTION('center_axis',(0.,-1.,0.));
#8068=DIRECTION('ref_axis',(1.,0.,0.));
#8069=DIRECTION('',(-0.707106781186547,0.707106781186548,-8.65956056235493E-17));
#8070=DIRECTION('center_axis',(0.,-1.,0.));
#8071=DIRECTION('ref_axis',(0.,0.,-1.));
#8072=DIRECTION('center_axis',(0.,-1.,0.));
#8073=DIRECTION('ref_axis',(1.,0.,0.));
#8074=DIRECTION('center_axis',(0.,1.,0.));
#8075=DIRECTION('ref_axis',(1.,0.,0.));
#8076=DIRECTION('center_axis',(0.,1.,0.));
#8077=DIRECTION('ref_axis',(1.,0.,0.));
#8078=DIRECTION('',(-0.447213595499958,0.894427190999916,-5.47678698264203E-17));
#8079=DIRECTION('center_axis',(0.,-1.,0.));
#8080=DIRECTION('ref_axis',(1.,0.,0.));
#8081=DIRECTION('center_axis',(0.,1.,0.));
#8082=DIRECTION('ref_axis',(1.,0.,0.));
#8083=DIRECTION('',(0.,1.,0.));
#8084=DIRECTION('center_axis',(0.,1.,0.));
#8085=DIRECTION('ref_axis',(1.,0.,0.));
#8086=DIRECTION('center_axis',(0.,-1.,0.));
#8087=DIRECTION('ref_axis',(1.,0.,0.));
#8088=DIRECTION('',(-0.707106781186547,0.707106781186548,-8.65956056235493E-17));
#8089=DIRECTION('center_axis',(0.,-1.,0.));
#8090=DIRECTION('ref_axis',(0.,0.,-1.));
#8091=DIRECTION('center_axis',(0.866025403784439,0.,-0.5));
#8092=DIRECTION('ref_axis',(0.5,0.,0.866025403784439));
#8093=DIRECTION('',(-0.5,0.,-0.866025403784439));
#8094=DIRECTION('',(0.,-1.,0.));
#8095=DIRECTION('',(0.5,0.,0.866025403784439));
#8096=DIRECTION('',(0.,-1.,0.));
#8097=DIRECTION('center_axis',(1.60246890531964E-16,0.,-1.));
#8098=DIRECTION('ref_axis',(1.,0.,1.60246890531964E-16));
#8099=DIRECTION('',(-1.,0.,-1.60246890531964E-16));
#8100=DIRECTION('',(0.,-1.,0.));
#8101=DIRECTION('',(1.,0.,1.60246890531964E-16));
#8102=DIRECTION('center_axis',(-0.866025403784439,0.,-0.5));
#8103=DIRECTION('ref_axis',(0.5,0.,-0.866025403784439));
#8104=DIRECTION('',(-0.5,0.,0.866025403784439));
#8105=DIRECTION('',(0.,-1.,0.));
#8106=DIRECTION('',(0.5,0.,-0.866025403784439));
#8107=DIRECTION('center_axis',(-0.866025403784439,0.,0.5));
#8108=DIRECTION('ref_axis',(-0.5,0.,-0.866025403784439));
#8109=DIRECTION('',(0.5,0.,0.866025403784439));
#8110=DIRECTION('',(0.,-1.,0.));
#8111=DIRECTION('',(-0.5,0.,-0.866025403784439));
#8112=DIRECTION('center_axis',(-1.60246890531964E-16,0.,1.));
#8113=DIRECTION('ref_axis',(-1.,0.,-1.60246890531964E-16));
#8114=DIRECTION('',(1.,0.,1.60246890531964E-16));
#8115=DIRECTION('',(0.,-1.,0.));
#8116=DIRECTION('',(-1.,0.,-1.60246890531964E-16));
#8117=DIRECTION('center_axis',(0.866025403784439,0.,0.5));
#8118=DIRECTION('ref_axis',(-0.5,0.,0.866025403784439));
#8119=DIRECTION('',(0.5,0.,-0.866025403784439));
#8120=DIRECTION('',(-0.5,0.,0.866025403784439));
#8121=DIRECTION('center_axis',(0.,1.,0.));
#8122=DIRECTION('ref_axis',(1.,0.,0.));
#8123=DIRECTION('center_axis',(0.,-1.,0.));
#8124=DIRECTION('ref_axis',(0.,0.,-1.));
#9821=CARTESIAN_POINT('',(0.,0.,0.));
#9822=CARTESIAN_POINT('Origin',(0.3,0.4,0.));
#9823=CARTESIAN_POINT('',(-0.3,0.4,-3.67394039744206E-17));
#9824=CARTESIAN_POINT('Origin',(0.,0.4,0.));
#9825=CARTESIAN_POINT('Origin',(0.,0.375,0.));
#9826=CARTESIAN_POINT('',(-0.35,0.35,-4.28626379701573E-17));
#9827=CARTESIAN_POINT('Origin',(0.,0.35,0.));
#9828=CARTESIAN_POINT('',(-0.325,0.375,-3.9801020972289E-17));
#9829=CARTESIAN_POINT('Origin',(0.,0.19,0.));
#9830=CARTESIAN_POINT('',(-0.35,0.03,-4.28626379701574E-17));
#9831=CARTESIAN_POINT('Origin',(0.,0.03,0.));
#9832=CARTESIAN_POINT('',(-0.35,0.19,-4.28626379701574E-17));
#9833=CARTESIAN_POINT('Origin',(0.,0.0149999999999999,0.));
#9834=CARTESIAN_POINT('',(-0.32,-3.29597460435593E-17,-3.91886975727153E-17));
#9835=CARTESIAN_POINT('Origin',(0.,0.,0.));
#9836=CARTESIAN_POINT('',(-0.335,0.0149999999999999,-4.10256677714363E-17));
#9837=CARTESIAN_POINT('Origin',(0.22,0.,0.));
#9838=CARTESIAN_POINT('',(-0.22,-6.93889390390723E-18,-2.69422295812418E-17));
#9839=CARTESIAN_POINT('Origin',(0.,0.,0.));
#9840=CARTESIAN_POINT('Origin',(0.,-0.02,0.));
#9841=CARTESIAN_POINT('',(-0.1954,-0.0492,2.39295984553393E-17));
#9842=CARTESIAN_POINT('Origin',(0.,-0.0492,0.));
#9843=CARTESIAN_POINT('',(-0.21,-0.02,-2.57175827820944E-17));
#9844=CARTESIAN_POINT('Origin',(0.,-0.8,0.));
#9845=CARTESIAN_POINT('',(-0.1954,-1.5646,2.39295984553393E-17));
#9846=CARTESIAN_POINT('Origin',(0.,-1.5646,0.));
#9847=CARTESIAN_POINT('',(-0.1954,-0.8,-2.39295984553393E-17));
#9848=CARTESIAN_POINT('Origin',(0.,-1.58,0.));
#9849=CARTESIAN_POINT('',(-0.16,-1.6,-1.95943487863577E-17));
#9850=CARTESIAN_POINT('Origin',(0.,-1.6,0.));
#9851=CARTESIAN_POINT('',(-0.18,-1.58,-2.20436423846524E-17));
#9852=CARTESIAN_POINT('Origin',(0.,-1.6,0.));
#9853=CARTESIAN_POINT('Origin',(0.0866025403784439,-0.4,-0.15));
#9854=CARTESIAN_POINT('',(0.173205080756888,-0.4,0.));
#9855=CARTESIAN_POINT('',(0.0866025403784439,-0.4,-0.15));
#9856=CARTESIAN_POINT('',(0.173205080756888,-0.4,0.));
#9857=CARTESIAN_POINT('',(0.0866025403784439,-0.64,-0.15));
#9858=CARTESIAN_POINT('',(0.0866025403784439,-0.4,-0.15));
#9859=CARTESIAN_POINT('',(0.173205080756888,-0.64,0.));
#9860=CARTESIAN_POINT('',(0.173205080756888,-0.64,0.));
#9861=CARTESIAN_POINT('',(0.173205080756888,-0.4,0.));
#9862=CARTESIAN_POINT('Origin',(-0.0866025403784438,-0.4,-0.15));
#9863=CARTESIAN_POINT('',(-0.0866025403784438,-0.4,-0.15));
#9864=CARTESIAN_POINT('',(0.0866025403784439,-0.4,-0.15));
#9865=CARTESIAN_POINT('',(-0.0866025403784438,-0.64,-0.15));
#9866=CARTESIAN_POINT('',(-0.0866025403784438,-0.4,-0.15));
#9867=CARTESIAN_POINT('',(0.0866025403784439,-0.64,-0.15));
#9868=CARTESIAN_POINT('Origin',(-0.173205080756888,-0.4,-2.77555756156289E-17));
#9869=CARTESIAN_POINT('',(-0.173205080756888,-0.4,-2.12115047744981E-17));
#9870=CARTESIAN_POINT('',(-0.0866025403784438,-0.4,-0.15));
#9871=CARTESIAN_POINT('',(-0.173205080756888,-0.64,-2.77555756156289E-17));
#9872=CARTESIAN_POINT('',(-0.173205080756888,-0.4,-2.12115047744981E-17));
#9873=CARTESIAN_POINT('',(-0.0866025403784438,-0.64,-0.15));
#9874=CARTESIAN_POINT('Origin',(-0.0866025403784439,-0.4,0.15));
#9875=CARTESIAN_POINT('',(-0.0866025403784439,-0.4,0.15));
#9876=CARTESIAN_POINT('',(-0.173205080756888,-0.4,-2.12115047744981E-17));
#9877=CARTESIAN_POINT('',(-0.0866025403784439,-0.64,0.15));
#9878=CARTESIAN_POINT('',(-0.0866025403784439,-0.4,0.15));
#9879=CARTESIAN_POINT('',(-0.173205080756888,-0.64,-2.12115047744981E-17));
#9880=CARTESIAN_POINT('Origin',(0.0866025403784439,-0.4,0.15));
#9881=CARTESIAN_POINT('',(0.0866025403784439,-0.4,0.15));
#9882=CARTESIAN_POINT('',(-0.0866025403784439,-0.4,0.15));
#9883=CARTESIAN_POINT('',(0.0866025403784439,-0.64,0.15));
#9884=CARTESIAN_POINT('',(0.0866025403784439,-0.4,0.15));
#9885=CARTESIAN_POINT('',(-0.0866025403784439,-0.64,0.15));
#9886=CARTESIAN_POINT('Origin',(0.173205080756888,-0.4,0.));
#9887=CARTESIAN_POINT('',(0.0866025403784439,-0.4,0.15));
#9888=CARTESIAN_POINT('',(0.0866025403784439,-0.64,0.15));
#9889=CARTESIAN_POINT('Origin',(0.,-0.4,-2.77555756156289E-17));
#9890=CARTESIAN_POINT('Origin',(0.,-0.64,-2.77555756156289E-17));
#10472=UNCERTAINTY_MEASURE_WITH_UNIT(LENGTH_MEASURE(0.001),#10518,
'DISTANCE_ACCURACY_VALUE',
'Maximum model space distance between geometric entities at asserted c
onnectivities');
#10484=UNCERTAINTY_MEASURE_WITH_UNIT(LENGTH_MEASURE(0.001),#10518,
'DISTANCE_ACCURACY_VALUE',
'Maximum model space distance between geometric entities at asserted c
onnectivities');
#10505=(
GEOMETRIC_REPRESENTATION_CONTEXT(3)
GLOBAL_UNCERTAINTY_ASSIGNED_CONTEXT((#10472))
GLOBAL_UNIT_ASSIGNED_CONTEXT((#10518,#10520,#10521))
REPRESENTATION_CONTEXT('','3D')
);
#10517=(
GEOMETRIC_REPRESENTATION_CONTEXT(3)
GLOBAL_UNCERTAINTY_ASSIGNED_CONTEXT((#10484))
GLOBAL_UNIT_ASSIGNED_CONTEXT((#10518,#10520,#10521))
REPRESENTATION_CONTEXT('','3D')
);
#10518=(
LENGTH_UNIT()
NAMED_UNIT(*)
SI_UNIT(.CENTI.,.METRE.)
);
#10520=(
NAMED_UNIT(*)
PLANE_ANGLE_UNIT()
SI_UNIT($,.RADIAN.)
);
#10521=(
NAMED_UNIT(*)
SI_UNIT($,.STERADIAN.)
SOLID_ANGLE_UNIT()
);
#10542=SHAPE_DEFINITION_REPRESENTATION(#10574,#10661);
#10574=PRODUCT_DEFINITION_SHAPE('',$,#10694);
#10661=SHAPE_REPRESENTATION('',(#6653),#10505);
#10673=PRODUCT_DEFINITION_CONTEXT('part definition',#10771,'design');
#10694=PRODUCT_DEFINITION('Cap Screw - M4x16','Cap Screw - M4x16',#10726,
#10673);
#10726=PRODUCT_DEFINITION_FORMATION('',$,#10793);
#10771=APPLICATION_CONTEXT(
'Core Data for Automotive Mechanical Design Process');
#10772=PRODUCT_CONTEXT('part definition',#10771,'mechanical');
#10793=PRODUCT('Cap Screw - M4x16','Cap Screw - M4x16',
'Cap Screw - M4x16',(#10772));
#10875=COLOUR_RGB('Black',0.12,0.14,0.17);
#10876=FILL_AREA_STYLE_COLOUR('',#10875);
#10877=FILL_AREA_STYLE('',(#10876));
#10878=SURFACE_STYLE_FILL_AREA(#10877);
#10879=SURFACE_SIDE_STYLE('',(#10878));
#10880=SURFACE_STYLE_USAGE(.BOTH.,#10879);
#10881=PRESENTATION_STYLE_ASSIGNMENT((#10880));
ENDSEC;
END-ISO-10303-21;
